ISO-10303-21;
HEADER;
/* Generated by software containing ST-Developer
 * from STEP Tools, Inc. (www.steptools.com) 
 */

FILE_DESCRIPTION(
/* description */ ('Shaft runout checking stand'),
/* implementation_level */ '2;1');

FILE_NAME(
/* name */ 'M4x10 Cap Screw.step',
/* time_stamp */ '2026-11-02T21:12:33-08:00',
/* author */ (''),
/* organization */ (''),
/* preprocessor_version */ 'ST-DEVELOPER v20.2',
/* originating_system */ 'Autodesk Translation Framework v15.17.0.0',
/* authorisation */ '');

FILE_SCHEMA (('AUTOMOTIVE_DESIGN { 1 0 10303 214 3 1 1 }'));
ENDSEC;

DATA;
#10=MECHANICAL_DESIGN_GEOMETRIC_PRESENTATION_REPRESENTATION('',(#485),#11748);
#354=ORIENTED_CLOSED_SHELL('',*,#6229,.F.);
#357=BREP_WITH_VOIDS('Body1',#6230,(#354));
#363=CONICAL_SURFACE('',#7099,0.325,0.785398163397448);
#364=CONICAL_SURFACE('',#7103,0.335,0.785398163397448);
#365=CONICAL_SURFACE('',#7107,0.21,0.463647609000806);
#399=SHAPE_REPRESENTATION_RELATIONSHIP('SRR','None',#11948,#442);
#442=ADVANCED_BREP_SHAPE_REPRESENTATION('',(#357),#11724);
#485=STYLED_ITEM('',(#12172),#357);
#634=FACE_BOUND('',#1696,.T.);
#795=CIRCLE('',#7096,0.1954);
#796=CIRCLE('',#7098,0.3);
#797=CIRCLE('',#7100,0.35);
#798=CIRCLE('',#7102,0.35);
#799=CIRCLE('',#7104,0.32);
#800=CIRCLE('',#7106,0.22);
#801=CIRCLE('',#7108,0.1954);
#996=CYLINDRICAL_SURFACE('',#7101,0.35);
#997=CYLINDRICAL_SURFACE('',#7109,0.1954);
#1242=FACE_OUTER_BOUND('',#1682,.T.);
#1243=FACE_OUTER_BOUND('',#1683,.T.);
#1244=FACE_OUTER_BOUND('',#1684,.T.);
#1245=FACE_OUTER_BOUND('',#1685,.T.);
#1246=FACE_OUTER_BOUND('',#1686,.T.);
#1247=FACE_OUTER_BOUND('',#1687,.T.);
#1248=FACE_OUTER_BOUND('',#1688,.T.);
#1249=FACE_OUTER_BOUND('',#1689,.T.);
#1250=FACE_OUTER_BOUND('',#1690,.T.);
#1251=FACE_OUTER_BOUND('',#1691,.T.);
#1252=FACE_OUTER_BOUND('',#1692,.T.);
#1253=FACE_OUTER_BOUND('',#1693,.T.);
#1254=FACE_OUTER_BOUND('',#1694,.T.);
#1255=FACE_OUTER_BOUND('',#1695,.T.);
#1256=FACE_OUTER_BOUND('',#1697,.T.);
#1257=FACE_OUTER_BOUND('',#1698,.T.);
#1682=EDGE_LOOP('',(#4980,#4981,#4982,#4983));
#1683=EDGE_LOOP('',(#4984,#4985,#4986,#4987));
#1684=EDGE_LOOP('',(#4988,#4989,#4990,#4991));
#1685=EDGE_LOOP('',(#4992,#4993,#4994,#4995));
#1686=EDGE_LOOP('',(#4996,#4997,#4998,#4999));
#1687=EDGE_LOOP('',(#5000,#5001,#5002,#5003));
#1688=EDGE_LOOP('',(#5004,#5005,#5006,#5007,#5008,#5009));
#1689=EDGE_LOOP('',(#5010,#5011,#5012,#5013,#5014,#5015));
#1690=EDGE_LOOP('',(#5016));
#1691=EDGE_LOOP('',(#5017));
#1692=EDGE_LOOP('',(#5018,#5019,#5020,#5021));
#1693=EDGE_LOOP('',(#5022,#5023,#5024,#5025));
#1694=EDGE_LOOP('',(#5026,#5027,#5028,#5029));
#1695=EDGE_LOOP('',(#5030));
#1696=EDGE_LOOP('',(#5031));
#1697=EDGE_LOOP('',(#5032,#5033,#5034,#5035));
#1698=EDGE_LOOP('',(#5036,#5037,#5038,#5039));
#2207=LINE('',#10449,#2674);
#2208=LINE('',#10451,#2675);
#2209=LINE('',#10453,#2676);
#2210=LINE('',#10454,#2677);
#2211=LINE('',#10457,#2678);
#2212=LINE('',#10459,#2679);
#2213=LINE('',#10460,#2680);
#2214=LINE('',#10463,#2681);
#2215=LINE('',#10465,#2682);
#2216=LINE('',#10466,#2683);
#2217=LINE('',#10469,#2684);
#2218=LINE('',#10471,#2685);
#2219=LINE('',#10472,#2686);
#2220=LINE('',#10475,#2687);
#2221=LINE('',#10477,#2688);
#2222=LINE('',#10478,#2689);
#2223=LINE('',#10480,#2690);
#2224=LINE('',#10481,#2691);
#2225=LINE('',#10493,#2692);
#2226=LINE('',#10497,#2693);
#2227=LINE('',#10501,#2694);
#2228=LINE('',#10508,#2695);
#2229=LINE('',#10510,#2696);
#2674=VECTOR('',#8522,1.);
#2675=VECTOR('',#8523,1.);
#2676=VECTOR('',#8524,1.);
#2677=VECTOR('',#8525,1.);
#2678=VECTOR('',#8528,1.);
#2679=VECTOR('',#8529,1.);
#2680=VECTOR('',#8530,1.);
#2681=VECTOR('',#8533,1.);
#2682=VECTOR('',#8534,1.);
#2683=VECTOR('',#8535,1.);
#2684=VECTOR('',#8538,1.);
#2685=VECTOR('',#8539,1.);
#2686=VECTOR('',#8540,1.);
#2687=VECTOR('',#8543,1.);
#2688=VECTOR('',#8544,1.);
#2689=VECTOR('',#8545,1.);
#2690=VECTOR('',#8548,1.);
#2691=VECTOR('',#8549,1.);
#2692=VECTOR('',#8566,0.325);
#2693=VECTOR('',#8571,0.35);
#2694=VECTOR('',#8576,0.335);
#2695=VECTOR('',#8585,0.21);
#2696=VECTOR('',#8588,0.2);
#3115=VERTEX_POINT('',#10447);
#3116=VERTEX_POINT('',#10448);
#3117=VERTEX_POINT('',#10450);
#3118=VERTEX_POINT('',#10452);
#3119=VERTEX_POINT('',#10456);
#3120=VERTEX_POINT('',#10458);
#3121=VERTEX_POINT('',#10462);
#3122=VERTEX_POINT('',#10464);
#3123=VERTEX_POINT('',#10468);
#3124=VERTEX_POINT('',#10470);
#3125=VERTEX_POINT('',#10474);
#3126=VERTEX_POINT('',#10476);
#3127=VERTEX_POINT('',#10485);
#3128=VERTEX_POINT('',#10488);
#3129=VERTEX_POINT('',#10491);
#3130=VERTEX_POINT('',#10495);
#3131=VERTEX_POINT('',#10499);
#3132=VERTEX_POINT('',#10503);
#3133=VERTEX_POINT('',#10506);
#3776=EDGE_CURVE('',#3115,#3116,#2207,.T.);
#3777=EDGE_CURVE('',#3116,#3117,#2208,.T.);
#3778=EDGE_CURVE('',#3117,#3118,#2209,.T.);
#3779=EDGE_CURVE('',#3115,#3118,#2210,.T.);
#3780=EDGE_CURVE('',#3116,#3119,#2211,.T.);
#3781=EDGE_CURVE('',#3119,#3120,#2212,.T.);
#3782=EDGE_CURVE('',#3120,#3117,#2213,.T.);
#3783=EDGE_CURVE('',#3119,#3121,#2214,.T.);
#3784=EDGE_CURVE('',#3121,#3122,#2215,.T.);
#3785=EDGE_CURVE('',#3122,#3120,#2216,.T.);
#3786=EDGE_CURVE('',#3121,#3123,#2217,.T.);
#3787=EDGE_CURVE('',#3123,#3124,#2218,.T.);
#3788=EDGE_CURVE('',#3124,#3122,#2219,.T.);
#3789=EDGE_CURVE('',#3123,#3125,#2220,.T.);
#3790=EDGE_CURVE('',#3125,#3126,#2221,.T.);
#3791=EDGE_CURVE('',#3126,#3124,#2222,.T.);
#3792=EDGE_CURVE('',#3125,#3115,#2223,.T.);
#3793=EDGE_CURVE('',#3118,#3126,#2224,.T.);
#3794=EDGE_CURVE('',#3127,#3127,#795,.T.);
#3795=EDGE_CURVE('',#3128,#3128,#796,.T.);
#3796=EDGE_CURVE('',#3129,#3129,#797,.T.);
#3797=EDGE_CURVE('',#3129,#3128,#2225,.T.);
#3798=EDGE_CURVE('',#3130,#3130,#798,.T.);
#3799=EDGE_CURVE('',#3130,#3129,#2226,.T.);
#3800=EDGE_CURVE('',#3131,#3131,#799,.T.);
#3801=EDGE_CURVE('',#3131,#3130,#2227,.T.);
#3802=EDGE_CURVE('',#3132,#3132,#800,.T.);
#3803=EDGE_CURVE('',#3133,#3133,#801,.F.);
#3804=EDGE_CURVE('',#3133,#3132,#2228,.T.);
#3805=EDGE_CURVE('',#3127,#3133,#2229,.T.);
#4980=ORIENTED_EDGE('',*,*,#3776,.T.);
#4981=ORIENTED_EDGE('',*,*,#3777,.T.);
#4982=ORIENTED_EDGE('',*,*,#3778,.T.);
#4983=ORIENTED_EDGE('',*,*,#3779,.F.);
#4984=ORIENTED_EDGE('',*,*,#3780,.T.);
#4985=ORIENTED_EDGE('',*,*,#3781,.T.);
#4986=ORIENTED_EDGE('',*,*,#3782,.T.);
#4987=ORIENTED_EDGE('',*,*,#3777,.F.);
#4988=ORIENTED_EDGE('',*,*,#3783,.T.);
#4989=ORIENTED_EDGE('',*,*,#3784,.T.);
#4990=ORIENTED_EDGE('',*,*,#3785,.T.);
#4991=ORIENTED_EDGE('',*,*,#3781,.F.);
#4992=ORIENTED_EDGE('',*,*,#3786,.T.);
#4993=ORIENTED_EDGE('',*,*,#3787,.T.);
#4994=ORIENTED_EDGE('',*,*,#3788,.T.);
#4995=ORIENTED_EDGE('',*,*,#3784,.F.);
#4996=ORIENTED_EDGE('',*,*,#3789,.T.);
#4997=ORIENTED_EDGE('',*,*,#3790,.T.);
#4998=ORIENTED_EDGE('',*,*,#3791,.T.);
#4999=ORIENTED_EDGE('',*,*,#3787,.F.);
#5000=ORIENTED_EDGE('',*,*,#3792,.T.);
#5001=ORIENTED_EDGE('',*,*,#3779,.T.);
#5002=ORIENTED_EDGE('',*,*,#3793,.T.);
#5003=ORIENTED_EDGE('',*,*,#3790,.F.);
#5004=ORIENTED_EDGE('',*,*,#3792,.F.);
#5005=ORIENTED_EDGE('',*,*,#3789,.F.);
#5006=ORIENTED_EDGE('',*,*,#3786,.F.);
#5007=ORIENTED_EDGE('',*,*,#3783,.F.);
#5008=ORIENTED_EDGE('',*,*,#3780,.F.);
#5009=ORIENTED_EDGE('',*,*,#3776,.F.);
#5010=ORIENTED_EDGE('',*,*,#3793,.F.);
#5011=ORIENTED_EDGE('',*,*,#3778,.F.);
#5012=ORIENTED_EDGE('',*,*,#3782,.F.);
#5013=ORIENTED_EDGE('',*,*,#3785,.F.);
#5014=ORIENTED_EDGE('',*,*,#3788,.F.);
#5015=ORIENTED_EDGE('',*,*,#3791,.F.);
#5016=ORIENTED_EDGE('',*,*,#3794,.F.);
#5017=ORIENTED_EDGE('',*,*,#3795,.F.);
#5018=ORIENTED_EDGE('',*,*,#3796,.F.);
#5019=ORIENTED_EDGE('',*,*,#3797,.T.);
#5020=ORIENTED_EDGE('',*,*,#3795,.T.);
#5021=ORIENTED_EDGE('',*,*,#3797,.F.);
#5022=ORIENTED_EDGE('',*,*,#3798,.F.);
#5023=ORIENTED_EDGE('',*,*,#3799,.T.);
#5024=ORIENTED_EDGE('',*,*,#3796,.T.);
#5025=ORIENTED_EDGE('',*,*,#3799,.F.);
#5026=ORIENTED_EDGE('',*,*,#3800,.F.);
#5027=ORIENTED_EDGE('',*,*,#3801,.T.);
#5028=ORIENTED_EDGE('',*,*,#3798,.T.);
#5029=ORIENTED_EDGE('',*,*,#3801,.F.);
#5030=ORIENTED_EDGE('',*,*,#3800,.T.);
#5031=ORIENTED_EDGE('',*,*,#3802,.F.);
#5032=ORIENTED_EDGE('',*,*,#3803,.F.);
#5033=ORIENTED_EDGE('',*,*,#3804,.T.);
#5034=ORIENTED_EDGE('',*,*,#3802,.T.);
#5035=ORIENTED_EDGE('',*,*,#3804,.F.);
#5036=ORIENTED_EDGE('',*,*,#3794,.T.);
#5037=ORIENTED_EDGE('',*,*,#3805,.T.);
#5038=ORIENTED_EDGE('',*,*,#3803,.T.);
#5039=ORIENTED_EDGE('',*,*,#3805,.F.);
#5746=PLANE('',#7087);
#5747=PLANE('',#7088);
#5748=PLANE('',#7089);
#5749=PLANE('',#7090);
#5750=PLANE('',#7091);
#5751=PLANE('',#7092);
#5752=PLANE('',#7093);
#5753=PLANE('',#7094);
#5754=PLANE('',#7095);
#5755=PLANE('',#7097);
#5756=PLANE('',#7105);
#6042=ADVANCED_FACE('',(#1242),#5746,.F.);
#6043=ADVANCED_FACE('',(#1243),#5747,.F.);
#6044=ADVANCED_FACE('',(#1244),#5748,.F.);
#6045=ADVANCED_FACE('',(#1245),#5749,.F.);
#6046=ADVANCED_FACE('',(#1246),#5750,.F.);
#6047=ADVANCED_FACE('',(#1247),#5751,.F.);
#6048=ADVANCED_FACE('',(#1248),#5752,.F.);
#6049=ADVANCED_FACE('',(#1249),#5753,.F.);
#6050=ADVANCED_FACE('',(#1250),#5754,.F.);
#6051=ADVANCED_FACE('',(#1251),#5755,.T.);
#6052=ADVANCED_FACE('',(#1252),#363,.T.);
#6053=ADVANCED_FACE('',(#1253),#996,.T.);
#6054=ADVANCED_FACE('',(#1254),#364,.T.);
#6055=ADVANCED_FACE('',(#1255,#634),#5756,.T.);
#6056=ADVANCED_FACE('',(#1256),#365,.T.);
#6057=ADVANCED_FACE('',(#1257),#997,.T.);
#6229=CLOSED_SHELL('',(#6042,#6043,#6044,#6045,#6046,#6047,#6048,#6049));
#6230=CLOSED_SHELL('',(#6050,#6051,#6052,#6053,#6054,#6055,#6056,#6057));
#7086=AXIS2_PLACEMENT_3D('',#10445,#8518,#8519);
#7087=AXIS2_PLACEMENT_3D('',#10446,#8520,#8521);
#7088=AXIS2_PLACEMENT_3D('',#10455,#8526,#8527);
#7089=AXIS2_PLACEMENT_3D('',#10461,#8531,#8532);
#7090=AXIS2_PLACEMENT_3D('',#10467,#8536,#8537);
#7091=AXIS2_PLACEMENT_3D('',#10473,#8541,#8542);
#7092=AXIS2_PLACEMENT_3D('',#10479,#8546,#8547);
#7093=AXIS2_PLACEMENT_3D('',#10482,#8550,#8551);
#7094=AXIS2_PLACEMENT_3D('',#10483,#8552,#8553);
#7095=AXIS2_PLACEMENT_3D('',#10484,#8554,#8555);
#7096=AXIS2_PLACEMENT_3D('',#10486,#8556,#8557);
#7097=AXIS2_PLACEMENT_3D('',#10487,#8558,#8559);
#7098=AXIS2_PLACEMENT_3D('',#10489,#8560,#8561);
#7099=AXIS2_PLACEMENT_3D('',#10490,#8562,#8563);
#7100=AXIS2_PLACEMENT_3D('',#10492,#8564,#8565);
#7101=AXIS2_PLACEMENT_3D('',#10494,#8567,#8568);
#7102=AXIS2_PLACEMENT_3D('',#10496,#8569,#8570);
#7103=AXIS2_PLACEMENT_3D('',#10498,#8572,#8573);
#7104=AXIS2_PLACEMENT_3D('',#10500,#8574,#8575);
#7105=AXIS2_PLACEMENT_3D('',#10502,#8577,#8578);
#7106=AXIS2_PLACEMENT_3D('',#10504,#8579,#8580);
#7107=AXIS2_PLACEMENT_3D('',#10505,#8581,#8582);
#7108=AXIS2_PLACEMENT_3D('',#10507,#8583,#8584);
#7109=AXIS2_PLACEMENT_3D('',#10509,#8586,#8587);
#8518=DIRECTION('axis',(0.,0.,1.));
#8519=DIRECTION('refdir',(1.,0.,0.));
#8520=DIRECTION('center_axis',(0.866025403784439,0.,-0.5));
#8521=DIRECTION('ref_axis',(0.5,0.,0.866025403784439));
#8522=DIRECTION('',(-0.5,0.,-0.866025403784439));
#8523=DIRECTION('',(0.,-1.,0.));
#8524=DIRECTION('',(0.5,0.,0.866025403784439));
#8525=DIRECTION('',(0.,-1.,0.));
#8526=DIRECTION('center_axis',(1.60246890531964E-16,0.,-1.));
#8527=DIRECTION('ref_axis',(1.,0.,1.60246890531964E-16));
#8528=DIRECTION('',(-1.,0.,-1.60246890531964E-16));
#8529=DIRECTION('',(0.,-1.,0.));
#8530=DIRECTION('',(1.,0.,1.60246890531964E-16));
#8531=DIRECTION('center_axis',(-0.866025403784439,0.,-0.5));
#8532=DIRECTION('ref_axis',(0.5,0.,-0.866025403784439));
#8533=DIRECTION('',(-0.5,0.,0.866025403784439));
#8534=DIRECTION('',(0.,-1.,0.));
#8535=DIRECTION('',(0.5,0.,-0.866025403784439));
#8536=DIRECTION('center_axis',(-0.866025403784439,0.,0.5));
#8537=DIRECTION('ref_axis',(-0.5,0.,-0.866025403784439));
#8538=DIRECTION('',(0.5,0.,0.866025403784439));
#8539=DIRECTION('',(0.,-1.,0.));
#8540=DIRECTION('',(-0.5,0.,-0.866025403784439));
#8541=DIRECTION('center_axis',(-1.60246890531964E-16,0.,1.));
#8542=DIRECTION('ref_axis',(-1.,0.,-1.60246890531964E-16));
#8543=DIRECTION('',(1.,0.,1.60246890531964E-16));
#8544=DIRECTION('',(0.,-1.,0.));
#8545=DIRECTION('',(-1.,0.,-1.60246890531964E-16));
#8546=DIRECTION('center_axis',(0.866025403784439,0.,0.5));
#8547=DIRECTION('ref_axis',(-0.5,0.,0.866025403784439));
#8548=DIRECTION('',(0.5,0.,-0.866025403784439));
#8549=DIRECTION('',(-0.5,0.,0.866025403784439));
#8550=DIRECTION('center_axis',(0.,1.,0.));
#8551=DIRECTION('ref_axis',(1.,0.,0.));
#8552=DIRECTION('center_axis',(0.,-1.,0.));
#8553=DIRECTION('ref_axis',(0.,0.,-1.));
#8554=DIRECTION('center_axis',(0.,1.,0.));
#8555=DIRECTION('ref_axis',(1.,0.,0.));
#8556=DIRECTION('center_axis',(0.,1.,0.));
#8557=DIRECTION('ref_axis',(1.,0.,0.));
#8558=DIRECTION('center_axis',(0.,1.,0.));
#8559=DIRECTION('ref_axis',(0.,0.,1.));
#8560=DIRECTION('center_axis',(0.,-1.,0.));
#8561=DIRECTION('ref_axis',(1.,0.,0.));
#8562=DIRECTION('center_axis',(0.,-1.,0.));
#8563=DIRECTION('ref_axis',(1.,0.,0.));
#8564=DIRECTION('center_axis',(0.,-1.,0.));
#8565=DIRECTION('ref_axis',(1.,0.,0.));
#8566=DIRECTION('',(0.707106781186547,0.707106781186548,8.65956056235493E-17));
#8567=DIRECTION('center_axis',(0.,-1.,0.));
#8568=DIRECTION('ref_axis',(1.,0.,0.));
#8569=DIRECTION('center_axis',(0.,-1.,0.));
#8570=DIRECTION('ref_axis',(1.,0.,0.));
#8571=DIRECTION('',(0.,1.,0.));
#8572=DIRECTION('center_axis',(0.,1.,0.));
#8573=DIRECTION('ref_axis',(1.,0.,0.));
#8574=DIRECTION('center_axis',(0.,-1.,0.));
#8575=DIRECTION('ref_axis',(1.,0.,0.));
#8576=DIRECTION('',(-0.707106781186547,0.707106781186548,-8.65956056235493E-17));
#8577=DIRECTION('center_axis',(0.,-1.,0.));
#8578=DIRECTION('ref_axis',(0.,0.,-1.));
#8579=DIRECTION('center_axis',(0.,-1.,0.));
#8580=DIRECTION('ref_axis',(1.,0.,0.));
#8581=DIRECTION('center_axis',(0.,1.,0.));
#8582=DIRECTION('ref_axis',(1.,0.,0.));
#8583=DIRECTION('center_axis',(0.,1.,0.));
#8584=DIRECTION('ref_axis',(1.,0.,0.));
#8585=DIRECTION('',(-0.447213595499958,0.894427190999916,-5.47678698264203E-17));
#8586=DIRECTION('center_axis',(0.,-1.,0.));
#8587=DIRECTION('ref_axis',(1.,0.,0.));
#8588=DIRECTION('',(0.,1.,0.));
#10445=CARTESIAN_POINT('',(0.,0.,0.));
#10446=CARTESIAN_POINT('Origin',(0.0866025403784439,-0.4,-0.15));
#10447=CARTESIAN_POINT('',(0.173205080756888,-0.4,0.));
#10448=CARTESIAN_POINT('',(0.0866025403784439,-0.4,-0.15));
#10449=CARTESIAN_POINT('',(0.173205080756888,-0.4,0.));
#10450=CARTESIAN_POINT('',(0.0866025403784439,-0.64,-0.15));
#10451=CARTESIAN_POINT('',(0.0866025403784439,-0.4,-0.15));
#10452=CARTESIAN_POINT('',(0.173205080756888,-0.64,0.));
#10453=CARTESIAN_POINT('',(0.173205080756888,-0.64,0.));
#10454=CARTESIAN_POINT('',(0.173205080756888,-0.4,0.));
#10455=CARTESIAN_POINT('Origin',(-0.0866025403784438,-0.4,-0.15));
#10456=CARTESIAN_POINT('',(-0.0866025403784438,-0.4,-0.15));
#10457=CARTESIAN_POINT('',(0.0866025403784439,-0.4,-0.15));
#10458=CARTESIAN_POINT('',(-0.0866025403784438,-0.64,-0.15));
#10459=CARTESIAN_POINT('',(-0.0866025403784438,-0.4,-0.15));
#10460=CARTESIAN_POINT('',(0.0866025403784439,-0.64,-0.15));
#10461=CARTESIAN_POINT('Origin',(-0.173205080756888,-0.4,-2.77555756156289E-17));
#10462=CARTESIAN_POINT('',(-0.173205080756888,-0.4,-2.12115047744981E-17));
#10463=CARTESIAN_POINT('',(-0.0866025403784438,-0.4,-0.15));
#10464=CARTESIAN_POINT('',(-0.173205080756888,-0.64,-2.77555756156289E-17));
#10465=CARTESIAN_POINT('',(-0.173205080756888,-0.4,-2.12115047744981E-17));
#10466=CARTESIAN_POINT('',(-0.0866025403784438,-0.64,-0.15));
#10467=CARTESIAN_POINT('Origin',(-0.0866025403784439,-0.4,0.15));
#10468=CARTESIAN_POINT('',(-0.0866025403784439,-0.4,0.15));
#10469=CARTESIAN_POINT('',(-0.173205080756888,-0.4,-2.12115047744981E-17));
#10470=CARTESIAN_POINT('',(-0.0866025403784439,-0.64,0.15));
#10471=CARTESIAN_POINT('',(-0.0866025403784439,-0.4,0.15));
#10472=CARTESIAN_POINT('',(-0.173205080756888,-0.64,-2.12115047744981E-17));
#10473=CARTESIAN_POINT('Origin',(0.0866025403784439,-0.4,0.15));
#10474=CARTESIAN_POINT('',(0.0866025403784439,-0.4,0.15));
#10475=CARTESIAN_POINT('',(-0.0866025403784439,-0.4,0.15));
#10476=CARTESIAN_POINT('',(0.0866025403784439,-0.64,0.15));
#10477=CARTESIAN_POINT('',(0.0866025403784439,-0.4,0.15));
#10478=CARTESIAN_POINT('',(-0.0866025403784439,-0.64,0.15));
#10479=CARTESIAN_POINT('Origin',(0.173205080756888,-0.4,0.));
#10480=CARTESIAN_POINT('',(0.0866025403784439,-0.4,0.15));
#10481=CARTESIAN_POINT('',(0.0866025403784439,-0.64,0.15));
#10482=CARTESIAN_POINT('Origin',(0.,-0.4,-2.77555756156289E-17));
#10483=CARTESIAN_POINT('Origin',(0.,-0.64,-2.77555756156289E-17));
#10484=CARTESIAN_POINT('Origin',(0.,-1.,0.));
#10485=CARTESIAN_POINT('',(-0.1954,-1.,2.39295984553393E-17));
#10486=CARTESIAN_POINT('Origin',(0.,-1.,0.));
#10487=CARTESIAN_POINT('Origin',(0.3,0.4,0.));
#10488=CARTESIAN_POINT('',(-0.3,0.4,-3.67394039744206E-17));
#10489=CARTESIAN_POINT('Origin',(0.,0.4,0.));
#10490=CARTESIAN_POINT('Origin',(0.,0.375,0.));
#10491=CARTESIAN_POINT('',(-0.35,0.35,-4.28626379701573E-17));
#10492=CARTESIAN_POINT('Origin',(0.,0.35,0.));
#10493=CARTESIAN_POINT('',(-0.325,0.375,-3.9801020972289E-17));
#10494=CARTESIAN_POINT('Origin',(0.,0.19,0.));
#10495=CARTESIAN_POINT('',(-0.35,0.03,-4.28626379701574E-17));
#10496=CARTESIAN_POINT('Origin',(0.,0.03,0.));
#10497=CARTESIAN_POINT('',(-0.35,0.19,-4.28626379701574E-17));
#10498=CARTESIAN_POINT('Origin',(0.,0.0149999999999999,0.));
#10499=CARTESIAN_POINT('',(-0.32,-3.29597460435593E-17,-3.91886975727153E-17));
#10500=CARTESIAN_POINT('Origin',(0.,0.,0.));
#10501=CARTESIAN_POINT('',(-0.335,0.0149999999999999,-4.10256677714363E-17));
#10502=CARTESIAN_POINT('Origin',(0.22,0.,0.));
#10503=CARTESIAN_POINT('',(-0.22,-6.93889390390723E-18,-2.69422295812418E-17));
#10504=CARTESIAN_POINT('Origin',(0.,0.,0.));
#10505=CARTESIAN_POINT('Origin',(0.,-0.02,0.));
#10506=CARTESIAN_POINT('',(-0.1954,-0.0492,2.39295984553393E-17));
#10507=CARTESIAN_POINT('Origin',(0.,-0.0492,0.));
#10508=CARTESIAN_POINT('',(-0.21,-0.02,-2.57175827820944E-17));
#10509=CARTESIAN_POINT('Origin',(0.,-0.8,0.));
#10510=CARTESIAN_POINT('',(-0.1954,-0.8,-2.39295984553393E-17));
#11675=UNCERTAINTY_MEASURE_WITH_UNIT(LENGTH_MEASURE(0.001),#11749,
'DISTANCE_ACCURACY_VALUE',
'Maximum model space distance between geometric entities at asserted c
onnectivities');
#11699=UNCERTAINTY_MEASURE_WITH_UNIT(LENGTH_MEASURE(0.001),#11749,
'DISTANCE_ACCURACY_VALUE',
'Maximum model space distance between geometric entities at asserted c
onnectivities');
#11724=(
GEOMETRIC_REPRESENTATION_CONTEXT(3)
GLOBAL_UNCERTAINTY_ASSIGNED_CONTEXT((#11675))
GLOBAL_UNIT_ASSIGNED_CONTEXT((#11749,#11751,#11752))
REPRESENTATION_CONTEXT('','3D')
);
#11748=(
GEOMETRIC_REPRESENTATION_CONTEXT(3)
GLOBAL_UNCERTAINTY_ASSIGNED_CONTEXT((#11699))
GLOBAL_UNIT_ASSIGNED_CONTEXT((#11749,#11751,#11752))
REPRESENTATION_CONTEXT('','3D')
);
#11749=(
LENGTH_UNIT()
NAMED_UNIT(*)
SI_UNIT(.CENTI.,.METRE.)
);
#11751=(
NAMED_UNIT(*)
PLANE_ANGLE_UNIT()
SI_UNIT($,.RADIAN.)
);
#11752=(
NAMED_UNIT(*)
SI_UNIT($,.STERADIAN.)
SOLID_ANGLE_UNIT()
);
#11777=SHAPE_DEFINITION_REPRESENTATION(#11825,#11948);
#11825=PRODUCT_DEFINITION_SHAPE('',$,#11997);
#11948=SHAPE_REPRESENTATION('',(#7086),#11724);
#11972=PRODUCT_DEFINITION_CONTEXT('part definition',#12118,'design');
#11997=PRODUCT_DEFINITION('M4x10 Cap Screw','M4x10 Cap Screw',#12045,#11972);
#12045=PRODUCT_DEFINITION_FORMATION('',$,#12144);
#12118=APPLICATION_CONTEXT(
'Core Data for Automotive Mechanical Design Process');
#12119=PRODUCT_CONTEXT('part definition',#12118,'mechanical');
#12144=PRODUCT('M4x10 Cap Screw','M4x10 Cap Screw','M4x10 Cap Screw',(#12119));
#12172=PRESENTATION_STYLE_ASSIGNMENT((#12177));
#12177=SURFACE_STYLE_USAGE(.BOTH.,#12182);
#12182=SURFACE_SIDE_STYLE('',(#12187));
#12187=SURFACE_STYLE_FILL_AREA(#12192);
#12192=FILL_AREA_STYLE('CAD Library Painted - Graphite',(#12197));
#12197=FILL_AREA_STYLE_COLOUR('CAD Library Painted - Graphite',#12202);
#12202=COLOUR_RGB('CAD Library Painted - Graphite',0.168627450980392,0.192156862745098,
0.231372549019608);
ENDSEC;
END-ISO-10303-21;
